ISO-10303-21;
HEADER;
/* Generated by software containing ST-Developer
 * from STEP Tools, Inc. (www.steptools.com) 
 */

FILE_DESCRIPTION(
/* description */ ('PAT-083'),
/* implementation_level */ '2;1');

FILE_NAME(
/* name */ 'Bottom service plug.step',
/* time_stamp */ '2026-10-29T20:18:00-07:00',
/* author */ (''),
/* organization */ (''),
/* preprocessor_version */ 'ST-DEVELOPER v20.2',
/* originating_system */ 'Autodesk Translation Framework v15.17.0.0',
/* authorisation */ '');

FILE_SCHEMA (('AUTOMOTIVE_DESIGN { 1 0 10303 214 3 1 1 }'));
ENDSEC;

DATA;
#10=MECHANICAL_DESIGN_GEOMETRIC_PRESENTATION_REPRESENTATION('',(#233),#8428);
#185=SHAPE_REPRESENTATION_RELATIONSHIP('SRR','None',#8519,#209);
#209=ADVANCED_BREP_SHAPE_REPRESENTATION('',(#257),#8408);
#233=STYLED_ITEM('',(#8698),#257);
#257=MANIFOLD_SOLID_BREP('Body1',#3679);
#297=FACE_BOUND('',#807,.T.);
#390=PLANE('',#4068);
#391=PLANE('',#4073);
#392=PLANE('',#4076);
#551=FACE_OUTER_BOUND('',#806,.T.);
#552=FACE_OUTER_BOUND('',#808,.T.);
#553=FACE_OUTER_BOUND('',#809,.T.);
#554=FACE_OUTER_BOUND('',#810,.T.);
#555=FACE_OUTER_BOUND('',#811,.T.);
#806=EDGE_LOOP('',(#2684));
#807=EDGE_LOOP('',(#2685));
#808=EDGE_LOOP('',(#2686,#2687,#2688,#2689));
#809=EDGE_LOOP('',(#2690));
#810=EDGE_LOOP('',(#2691,#2692,#2693,#2694));
#811=EDGE_LOOP('',(#2695));
#1106=LINE('',#6011,#1350);
#1107=LINE('',#6017,#1351);
#1350=VECTOR('',#4712,1.3);
#1351=VECTOR('',#4721,1.);
#1570=CIRCLE('',#4069,1.3);
#1571=CIRCLE('',#4070,1.);
#1572=CIRCLE('',#4072,1.3);
#1573=CIRCLE('',#4075,1.);
#1783=VERTEX_POINT('',#6005);
#1784=VERTEX_POINT('',#6007);
#1785=VERTEX_POINT('',#6010);
#1786=VERTEX_POINT('',#6015);
#2118=EDGE_CURVE('',#1783,#1783,#1570,.T.);
#2119=EDGE_CURVE('',#1784,#1784,#1571,.T.);
#2120=EDGE_CURVE('',#1783,#1785,#1106,.T.);
#2121=EDGE_CURVE('',#1785,#1785,#1572,.T.);
#2122=EDGE_CURVE('',#1786,#1786,#1573,.T.);
#2123=EDGE_CURVE('',#1786,#1784,#1107,.T.);
#2684=ORIENTED_EDGE('',*,*,#2118,.T.);
#2685=ORIENTED_EDGE('',*,*,#2119,.F.);
#2686=ORIENTED_EDGE('',*,*,#2118,.F.);
#2687=ORIENTED_EDGE('',*,*,#2120,.T.);
#2688=ORIENTED_EDGE('',*,*,#2121,.T.);
#2689=ORIENTED_EDGE('',*,*,#2120,.F.);
#2690=ORIENTED_EDGE('',*,*,#2121,.F.);
#2691=ORIENTED_EDGE('',*,*,#2122,.F.);
#2692=ORIENTED_EDGE('',*,*,#2123,.T.);
#2693=ORIENTED_EDGE('',*,*,#2119,.T.);
#2694=ORIENTED_EDGE('',*,*,#2123,.F.);
#2695=ORIENTED_EDGE('',*,*,#2122,.T.);
#3386=CYLINDRICAL_SURFACE('',#4071,1.3);
#3387=CYLINDRICAL_SURFACE('',#4074,1.);
#3498=ADVANCED_FACE('',(#551,#297),#390,.T.);
#3499=ADVANCED_FACE('',(#552),#3386,.T.);
#3500=ADVANCED_FACE('',(#553),#391,.F.);
#3501=ADVANCED_FACE('',(#554),#3387,.T.);
#3502=ADVANCED_FACE('',(#555),#392,.T.);
#3679=CLOSED_SHELL('',(#3498,#3499,#3500,#3501,#3502));
#4067=AXIS2_PLACEMENT_3D('',#6003,#4702,#4703);
#4068=AXIS2_PLACEMENT_3D('',#6004,#4704,#4705);
#4069=AXIS2_PLACEMENT_3D('',#6006,#4706,#4707);
#4070=AXIS2_PLACEMENT_3D('',#6008,#4708,#4709);
#4071=AXIS2_PLACEMENT_3D('',#6009,#4710,#4711);
#4072=AXIS2_PLACEMENT_3D('',#6012,#4713,#4714);
#4073=AXIS2_PLACEMENT_3D('',#6013,#4715,#4716);
#4074=AXIS2_PLACEMENT_3D('',#6014,#4717,#4718);
#4075=AXIS2_PLACEMENT_3D('',#6016,#4719,#4720);
#4076=AXIS2_PLACEMENT_3D('',#6018,#4722,#4723);
#4702=DIRECTION('axis',(0.,0.,1.));
#4703=DIRECTION('refdir',(1.,0.,0.));
#4704=DIRECTION('center_axis',(0.,0.,1.));
#4705=DIRECTION('ref_axis',(1.,0.,0.));
#4706=DIRECTION('center_axis',(0.,0.,1.));
#4707=DIRECTION('ref_axis',(1.,0.,0.));
#4708=DIRECTION('center_axis',(0.,0.,1.));
#4709=DIRECTION('ref_axis',(1.,0.,0.));
#4710=DIRECTION('center_axis',(0.,0.,1.));
#4711=DIRECTION('ref_axis',(1.,0.,0.));
#4712=DIRECTION('',(0.,0.,-1.));
#4713=DIRECTION('center_axis',(0.,0.,1.));
#4714=DIRECTION('ref_axis',(1.,0.,0.));
#4715=DIRECTION('center_axis',(0.,0.,1.));
#4716=DIRECTION('ref_axis',(1.,0.,0.));
#4717=DIRECTION('center_axis',(0.,0.,1.));
#4718=DIRECTION('ref_axis',(1.,0.,0.));
#4719=DIRECTION('center_axis',(0.,0.,1.));
#4720=DIRECTION('ref_axis',(1.,0.,0.));
#4721=DIRECTION('',(0.,0.,-1.));
#4722=DIRECTION('center_axis',(0.,0.,1.));
#4723=DIRECTION('ref_axis',(1.,0.,0.));
#6003=CARTESIAN_POINT('',(0.,0.,0.));
#6004=CARTESIAN_POINT('Origin',(0.,0.,1.));
#6005=CARTESIAN_POINT('',(-1.3,-1.59204083889156E-16,1.));
#6006=CARTESIAN_POINT('Origin',(0.,0.,1.));
#6007=CARTESIAN_POINT('',(-1.,-1.22464679914735E-16,1.));
#6008=CARTESIAN_POINT('Origin',(0.,0.,1.));
#6009=CARTESIAN_POINT('Origin',(0.,0.,0.8));
#6010=CARTESIAN_POINT('',(-1.3,-1.59204083889156E-16,0.8));
#6011=CARTESIAN_POINT('',(-1.3,-1.59204083889156E-16,0.8));
#6012=CARTESIAN_POINT('Origin',(0.,0.,0.8));
#6013=CARTESIAN_POINT('Origin',(0.,0.,0.8));
#6014=CARTESIAN_POINT('Origin',(0.,0.,1.));
#6015=CARTESIAN_POINT('',(-1.,-1.22464679914735E-16,1.4));
#6016=CARTESIAN_POINT('Origin',(0.,0.,1.4));
#6017=CARTESIAN_POINT('',(-1.,-1.22464679914735E-16,1.));
#6018=CARTESIAN_POINT('Origin',(0.,0.,1.4));
#8382=UNCERTAINTY_MEASURE_WITH_UNIT(LENGTH_MEASURE(0.001),#8429,
'DISTANCE_ACCURACY_VALUE',
'Maximum model space distance between geometric entities at asserted c
onnectivities');
#8402=UNCERTAINTY_MEASURE_WITH_UNIT(LENGTH_MEASURE(0.001),#8429,
'DISTANCE_ACCURACY_VALUE',
'Maximum model space distance between geometric entities at asserted c
onnectivities');
#8408=(
GEOMETRIC_REPRESENTATION_CONTEXT(3)
GLOBAL_UNCERTAINTY_ASSIGNED_CONTEXT((#8382))
GLOBAL_UNIT_ASSIGNED_CONTEXT((#8429,#8431,#8432))
REPRESENTATION_CONTEXT('','3D')
);
#8428=(
GEOMETRIC_REPRESENTATION_CONTEXT(3)
GLOBAL_UNCERTAINTY_ASSIGNED_CONTEXT((#8402))
GLOBAL_UNIT_ASSIGNED_CONTEXT((#8429,#8431,#8432))
REPRESENTATION_CONTEXT('','3D')
);
#8429=(
LENGTH_UNIT()
NAMED_UNIT(*)
SI_UNIT(.CENTI.,.METRE.)
);
#8431=(
NAMED_UNIT(*)
PLANE_ANGLE_UNIT()
SI_UNIT($,.RADIAN.)
);
#8432=(
NAMED_UNIT(*)
SI_UNIT($,.STERADIAN.)
SOLID_ANGLE_UNIT()
);
#8438=SHAPE_DEFINITION_REPRESENTATION(#8463,#8519);
#8463=PRODUCT_DEFINITION_SHAPE('',$,#8545);
#8519=SHAPE_REPRESENTATION('',(#4067),#8408);
#8539=PRODUCT_DEFINITION_CONTEXT('part definition',#8616,'design');
#8545=PRODUCT_DEFINITION('Bottom service plug',
'Bottom service plug',#8570,#8539);
#8570=PRODUCT_DEFINITION_FORMATION('',$,#8623);
#8616=APPLICATION_CONTEXT(
'Core Data for Automotive Mechanical Design Process');
#8617=PRODUCT_CONTEXT('part definition',#8616,'mechanical');
#8623=PRODUCT('Bottom service plug','Bottom service plug',
'Bottom service plug',(#8617));
#8692=COLOUR_RGB('Sky Blue',0.24,0.69,0.87);
#8693=FILL_AREA_STYLE_COLOUR('',#8692);
#8694=FILL_AREA_STYLE('',(#8693));
#8695=SURFACE_STYLE_FILL_AREA(#8694);
#8696=SURFACE_SIDE_STYLE('',(#8695));
#8697=SURFACE_STYLE_USAGE(.BOTH.,#8696);
#8698=PRESENTATION_STYLE_ASSIGNMENT((#8697));
ENDSEC;
END-ISO-10303-21;
